ISO-10303-21;
HEADER;
/* Generated by software containing ST-Developer
 * from STEP Tools, Inc. (www.steptools.com) 
 */

FILE_DESCRIPTION(
/* description */ ('Cable chain and bracket set'),
/* implementation_level */ '2;1');

FILE_NAME(
/* name */ 'Offset cable chain link__PD6081.step',
/* time_stamp */ '2026-10-29T17:19:47-07:00',
/* author */ (''),
/* organization */ (''),
/* preprocessor_version */ 'ST-DEVELOPER v20.2',
/* originating_system */ 'Autodesk Translation Framework v15.17.0.0',
/* authorisation */ '');

FILE_SCHEMA (('AUTOMOTIVE_DESIGN { 1 0 10303 214 3 1 1 }'));
ENDSEC;

DATA;
#10=MECHANICAL_DESIGN_GEOMETRIC_PRESENTATION_REPRESENTATION('',(#345),#5929);
#301=ELLIPSE('',#3644,0.415214835958447,0.41);
#302=ELLIPSE('',#3647,0.415214835958447,0.41);
#303=ELLIPSE('',#3653,0.415214835958447,0.41);
#304=ELLIPSE('',#3655,0.415214835958447,0.41);
#305=ELLIPSE('',#3658,0.415214835958447,0.41);
#306=ELLIPSE('',#3660,0.415214835958447,0.41);
#307=ELLIPSE('',#3666,0.708903378465641,0.7);
#308=ELLIPSE('',#3668,0.708903378465641,0.7);
#309=ELLIPSE('',#3679,0.708903378465641,0.7);
#310=ELLIPSE('',#3690,0.708903378465641,0.7);
#319=SHAPE_REPRESENTATION_RELATIONSHIP('SRR','None',#6057,#332);
#332=ADVANCED_BREP_SHAPE_REPRESENTATION('',(#358),#5924);
#345=STYLED_ITEM('',(#6234),#358);
#358=MANIFOLD_SOLID_BREP('Body1',#3339);
#393=FACE_BOUND('',#866,.T.);
#394=FACE_BOUND('',#877,.T.);
#395=FACE_BOUND('',#880,.T.);
#396=FACE_BOUND('',#889,.T.);
#483=PLANE('',#3661);
#484=PLANE('',#3663);
#485=PLANE('',#3665);
#486=PLANE('',#3667);
#487=PLANE('',#3669);
#488=PLANE('',#3670);
#489=PLANE('',#3671);
#490=PLANE('',#3672);
#491=PLANE('',#3677);
#492=PLANE('',#3680);
#493=PLANE('',#3681);
#494=PLANE('',#3682);
#495=PLANE('',#3683);
#496=PLANE('',#3688);
#497=PLANE('',#3689);
#498=PLANE('',#3691);
#499=PLANE('',#3697);
#500=PLANE('',#3698);
#501=PLANE('',#3699);
#502=PLANE('',#3700);
#503=PLANE('',#3701);
#504=PLANE('',#3702);
#642=FACE_OUTER_BOUND('',#854,.T.);
#643=FACE_OUTER_BOUND('',#855,.T.);
#644=FACE_OUTER_BOUND('',#856,.T.);
#645=FACE_OUTER_BOUND('',#857,.T.);
#646=FACE_OUTER_BOUND('',#858,.T.);
#647=FACE_OUTER_BOUND('',#859,.T.);
#648=FACE_OUTER_BOUND('',#860,.T.);
#649=FACE_OUTER_BOUND('',#861,.T.);
#650=FACE_OUTER_BOUND('',#862,.T.);
#651=FACE_OUTER_BOUND('',#863,.T.);
#652=FACE_OUTER_BOUND('',#864,.T.);
#653=FACE_OUTER_BOUND('',#865,.T.);
#654=FACE_OUTER_BOUND('',#867,.T.);
#655=FACE_OUTER_BOUND('',#868,.T.);
#656=FACE_OUTER_BOUND('',#869,.T.);
#657=FACE_OUTER_BOUND('',#870,.T.);
#658=FACE_OUTER_BOUND('',#871,.T.);
#659=FACE_OUTER_BOUND('',#872,.T.);
#660=FACE_OUTER_BOUND('',#873,.T.);
#661=FACE_OUTER_BOUND('',#874,.T.);
#662=FACE_OUTER_BOUND('',#875,.T.);
#663=FACE_OUTER_BOUND('',#876,.T.);
#664=FACE_OUTER_BOUND('',#878,.T.);
#665=FACE_OUTER_BOUND('',#879,.T.);
#666=FACE_OUTER_BOUND('',#881,.T.);
#667=FACE_OUTER_BOUND('',#882,.T.);
#668=FACE_OUTER_BOUND('',#883,.T.);
#669=FACE_OUTER_BOUND('',#884,.T.);
#670=FACE_OUTER_BOUND('',#885,.T.);
#671=FACE_OUTER_BOUND('',#886,.T.);
#672=FACE_OUTER_BOUND('',#887,.T.);
#673=FACE_OUTER_BOUND('',#888,.T.);
#674=FACE_OUTER_BOUND('',#890,.T.);
#675=FACE_OUTER_BOUND('',#891,.T.);
#854=EDGE_LOOP('',(#2799,#2800,#2801,#2802,#2803,#2804));
#855=EDGE_LOOP('',(#2805,#2806,#2807,#2808,#2809,#2810));
#856=EDGE_LOOP('',(#2811,#2812,#2813,#2814,#2815,#2816));
#857=EDGE_LOOP('',(#2817,#2818,#2819,#2820,#2821,#2822));
#858=EDGE_LOOP('',(#2823,#2824,#2825,#2826,#2827));
#859=EDGE_LOOP('',(#2828,#2829,#2830,#2831,#2832));
#860=EDGE_LOOP('',(#2833,#2834,#2835,#2836,#2837,#2838,#2839,#2840,#2841));
#861=EDGE_LOOP('',(#2842,#2843,#2844,#2845,#2846,#2847,#2848,#2849,#2850));
#862=EDGE_LOOP('',(#2851,#2852,#2853,#2854));
#863=EDGE_LOOP('',(#2855,#2856,#2857,#2858));
#864=EDGE_LOOP('',(#2859,#2860,#2861,#2862));
#865=EDGE_LOOP('',(#2863,#2864));
#866=EDGE_LOOP('',(#2865));
#867=EDGE_LOOP('',(#2866,#2867,#2868,#2869));
#868=EDGE_LOOP('',(#2870,#2871,#2872,#2873));
#869=EDGE_LOOP('',(#2874,#2875));
#870=EDGE_LOOP('',(#2876,#2877,#2878,#2879,#2880,#2881,#2882,#2883,#2884,
#2885,#2886,#2887));
#871=EDGE_LOOP('',(#2888,#2889,#2890,#2891));
#872=EDGE_LOOP('',(#2892,#2893,#2894,#2895));
#873=EDGE_LOOP('',(#2896,#2897,#2898,#2899));
#874=EDGE_LOOP('',(#2900,#2901));
#875=EDGE_LOOP('',(#2902,#2903,#2904,#2905));
#876=EDGE_LOOP('',(#2906,#2907));
#877=EDGE_LOOP('',(#2908));
#878=EDGE_LOOP('',(#2909,#2910,#2911,#2912,#2913,#2914,#2915,#2916,#2917,
#2918,#2919,#2920));
#879=EDGE_LOOP('',(#2921,#2922));
#880=EDGE_LOOP('',(#2923));
#881=EDGE_LOOP('',(#2924,#2925));
#882=EDGE_LOOP('',(#2926,#2927,#2928,#2929));
#883=EDGE_LOOP('',(#2930,#2931,#2932,#2933));
#884=EDGE_LOOP('',(#2934,#2935,#2936,#2937));
#885=EDGE_LOOP('',(#2938,#2939,#2940,#2941));
#886=EDGE_LOOP('',(#2942,#2943,#2944,#2945));
#887=EDGE_LOOP('',(#2946,#2947,#2948,#2949,#2950,#2951,#2952,#2953,#2954,
#2955,#2956,#2957));
#888=EDGE_LOOP('',(#2958,#2959));
#889=EDGE_LOOP('',(#2960));
#890=EDGE_LOOP('',(#2961,#2962));
#891=EDGE_LOOP('',(#2963,#2964,#2965,#2966));
#1112=LINE('',#5488,#1372);
#1113=LINE('',#5501,#1373);
#1114=LINE('',#5511,#1374);
#1115=LINE('',#5518,#1375);
#1116=LINE('',#5526,#1376);
#1117=LINE('',#5529,#1377);
#1118=LINE('',#5532,#1378);
#1119=LINE('',#5535,#1379);
#1120=LINE('',#5538,#1380);
#1121=LINE('',#5540,#1381);
#1122=LINE('',#5542,#1382);
#1123=LINE('',#5544,#1383);
#1124=LINE('',#5548,#1384);
#1125=LINE('',#5549,#1385);
#1126=LINE('',#5552,#1386);
#1127=LINE('',#5554,#1387);
#1128=LINE('',#5558,#1388);
#1129=LINE('',#5560,#1389);
#1130=LINE('',#5562,#1390);
#1131=LINE('',#5563,#1391);
#1132=LINE('',#5567,#1392);
#1133=LINE('',#5569,#1393);
#1134=LINE('',#5571,#1394);
#1135=LINE('',#5572,#1395);
#1136=LINE('',#5576,#1396);
#1137=LINE('',#5578,#1397);
#1138=LINE('',#5580,#1398);
#1139=LINE('',#5581,#1399);
#1140=LINE('',#5583,#1400);
#1141=LINE('',#5584,#1401);
#1142=LINE('',#5591,#1402);
#1143=LINE('',#5593,#1403);
#1144=LINE('',#5599,#1404);
#1145=LINE('',#5600,#1405);
#1146=LINE('',#5602,#1406);
#1147=LINE('',#5603,#1407);
#1148=LINE('',#5604,#1408);
#1149=LINE('',#5606,#1409);
#1150=LINE('',#5608,#1410);
#1151=LINE('',#5609,#1411);
#1152=LINE('',#5611,#1412);
#1153=LINE('',#5619,#1413);
#1154=LINE('',#5623,#1414);
#1155=LINE('',#5624,#1415);
#1156=LINE('',#5626,#1416);
#1157=LINE('',#5627,#1417);
#1158=LINE('',#5633,#1418);
#1159=LINE('',#5634,#1419);
#1160=LINE('',#5638,#1420);
#1161=LINE('',#5640,#1421);
#1162=LINE('',#5641,#1422);
#1163=LINE('',#5643,#1423);
#1372=VECTOR('',#4435,0.41);
#1373=VECTOR('',#4448,0.41);
#1374=VECTOR('',#4459,0.41);
#1375=VECTOR('',#4468,0.41);
#1376=VECTOR('',#4477,1.);
#1377=VECTOR('',#4480,1.);
#1378=VECTOR('',#4483,1.);
#1379=VECTOR('',#4486,1.);
#1380=VECTOR('',#4489,1.);
#1381=VECTOR('',#4490,1.);
#1382=VECTOR('',#4491,1.);
#1383=VECTOR('',#4492,1.);
#1384=VECTOR('',#4495,1.);
#1385=VECTOR('',#4496,1.);
#1386=VECTOR('',#4499,1.);
#1387=VECTOR('',#4500,1.);
#1388=VECTOR('',#4503,1.);
#1389=VECTOR('',#4504,1.);
#1390=VECTOR('',#4505,1.);
#1391=VECTOR('',#4506,1.);
#1392=VECTOR('',#4509,1.);
#1393=VECTOR('',#4510,1.);
#1394=VECTOR('',#4511,1.);
#1395=VECTOR('',#4512,1.);
#1396=VECTOR('',#4515,1.);
#1397=VECTOR('',#4516,1.);
#1398=VECTOR('',#4517,1.);
#1399=VECTOR('',#4518,1.);
#1400=VECTOR('',#4521,1.);
#1401=VECTOR('',#4522,1.);
#1402=VECTOR('',#4531,1.);
#1403=VECTOR('',#4534,1.);
#1404=VECTOR('',#4543,1.);
#1405=VECTOR('',#4544,1.);
#1406=VECTOR('',#4545,1.);
#1407=VECTOR('',#4546,1.);
#1408=VECTOR('',#4547,1.);
#1409=VECTOR('',#4550,1.);
#1410=VECTOR('',#4553,1.);
#1411=VECTOR('',#4554,1.);
#1412=VECTOR('',#4557,1.);
#1413=VECTOR('',#4570,1.);
#1414=VECTOR('',#4573,1.);
#1415=VECTOR('',#4574,1.);
#1416=VECTOR('',#4575,1.);
#1417=VECTOR('',#4576,1.);
#1418=VECTOR('',#4587,1.);
#1419=VECTOR('',#4588,1.);
#1420=VECTOR('',#4595,1.);
#1421=VECTOR('',#4598,1.);
#1422=VECTOR('',#4599,1.);
#1423=VECTOR('',#4602,1.);
#1521=CIRCLE('',#3642,0.41);
#1522=CIRCLE('',#3643,0.41);
#1523=CIRCLE('',#3645,0.41);
#1524=CIRCLE('',#3648,0.41);
#1525=CIRCLE('',#3649,0.41);
#1526=CIRCLE('',#3650,0.41);
#1527=CIRCLE('',#3652,0.41);
#1528=CIRCLE('',#3654,0.41);
#1529=CIRCLE('',#3657,0.41);
#1530=CIRCLE('',#3659,0.41);
#1531=CIRCLE('',#3662,0.7);
#1532=CIRCLE('',#3664,0.7);
#1533=CIRCLE('',#3673,0.7);
#1534=CIRCLE('',#3674,0.7);
#1535=CIRCLE('',#3676,0.7);
#1536=CIRCLE('',#3685,0.7);
#1537=CIRCLE('',#3687,0.7);
#1538=CIRCLE('',#3692,0.7);
#1539=CIRCLE('',#3693,0.7);
#1540=CIRCLE('',#3696,0.7);
#1541=CIRCLE('',#3703,0.7);
#1542=CIRCLE('',#3704,0.7);
#1735=VERTEX_POINT('',#5485);
#1736=VERTEX_POINT('',#5487);
#1737=VERTEX_POINT('',#5489);
#1738=VERTEX_POINT('',#5491);
#1739=VERTEX_POINT('',#5495);
#1740=VERTEX_POINT('',#5496);
#1741=VERTEX_POINT('',#5498);
#1742=VERTEX_POINT('',#5500);
#1743=VERTEX_POINT('',#5505);
#1744=VERTEX_POINT('',#5506);
#1745=VERTEX_POINT('',#5508);
#1746=VERTEX_POINT('',#5510);
#1747=VERTEX_POINT('',#5515);
#1748=VERTEX_POINT('',#5517);
#1749=VERTEX_POINT('',#5519);
#1750=VERTEX_POINT('',#5521);
#1751=VERTEX_POINT('',#5525);
#1752=VERTEX_POINT('',#5527);
#1753=VERTEX_POINT('',#5531);
#1754=VERTEX_POINT('',#5533);
#1755=VERTEX_POINT('',#5537);
#1756=VERTEX_POINT('',#5539);
#1757=VERTEX_POINT('',#5541);
#1758=VERTEX_POINT('',#5543);
#1759=VERTEX_POINT('',#5545);
#1760=VERTEX_POINT('',#5547);
#1761=VERTEX_POINT('',#5551);
#1762=VERTEX_POINT('',#5553);
#1763=VERTEX_POINT('',#5555);
#1764=VERTEX_POINT('',#5557);
#1765=VERTEX_POINT('',#5559);
#1766=VERTEX_POINT('',#5561);
#1767=VERTEX_POINT('',#5565);
#1768=VERTEX_POINT('',#5566);
#1769=VERTEX_POINT('',#5568);
#1770=VERTEX_POINT('',#5570);
#1771=VERTEX_POINT('',#5574);
#1772=VERTEX_POINT('',#5575);
#1773=VERTEX_POINT('',#5577);
#1774=VERTEX_POINT('',#5579);
#1775=VERTEX_POINT('',#5586);
#1776=VERTEX_POINT('',#5587);
#1777=VERTEX_POINT('',#5598);
#1778=VERTEX_POINT('',#5601);
#1779=VERTEX_POINT('',#5618);
#1780=VERTEX_POINT('',#5620);
#1781=VERTEX_POINT('',#5622);
#1782=VERTEX_POINT('',#5625);
#2100=EDGE_CURVE('',#1735,#1735,#1521,.T.);
#2101=EDGE_CURVE('',#1735,#1736,#1112,.T.);
#2102=EDGE_CURVE('',#1737,#1736,#1522,.T.);
#2103=EDGE_CURVE('',#1738,#1737,#301,.T.);
#2104=EDGE_CURVE('',#1736,#1738,#1523,.T.);
#2105=EDGE_CURVE('',#1739,#1740,#302,.T.);
#2106=EDGE_CURVE('',#1741,#1739,#1524,.T.);
#2107=EDGE_CURVE('',#1741,#1742,#1113,.T.);
#2108=EDGE_CURVE('',#1742,#1742,#1525,.T.);
#2109=EDGE_CURVE('',#1740,#1741,#1526,.T.);
#2110=EDGE_CURVE('',#1743,#1744,#1527,.T.);
#2111=EDGE_CURVE('',#1745,#1743,#303,.T.);
#2112=EDGE_CURVE('',#1745,#1746,#1114,.T.);
#2113=EDGE_CURVE('',#1746,#1746,#1528,.T.);
#2114=EDGE_CURVE('',#1744,#1745,#304,.T.);
#2115=EDGE_CURVE('',#1747,#1747,#1529,.T.);
#2116=EDGE_CURVE('',#1747,#1748,#1115,.T.);
#2117=EDGE_CURVE('',#1749,#1748,#305,.T.);
#2118=EDGE_CURVE('',#1750,#1749,#1530,.T.);
#2119=EDGE_CURVE('',#1748,#1750,#306,.T.);
#2120=EDGE_CURVE('',#1739,#1751,#1116,.T.);
#2121=EDGE_CURVE('',#1752,#1751,#1531,.T.);
#2122=EDGE_CURVE('',#1752,#1740,#1117,.T.);
#2123=EDGE_CURVE('',#1738,#1753,#1118,.T.);
#2124=EDGE_CURVE('',#1753,#1754,#1532,.T.);
#2125=EDGE_CURVE('',#1754,#1737,#1119,.T.);
#2126=EDGE_CURVE('',#1755,#1750,#1120,.T.);
#2127=EDGE_CURVE('',#1756,#1755,#1121,.T.);
#2128=EDGE_CURVE('',#1756,#1757,#1122,.T.);
#2129=EDGE_CURVE('',#1757,#1758,#1123,.T.);
#2130=EDGE_CURVE('',#1759,#1758,#307,.T.);
#2131=EDGE_CURVE('',#1760,#1759,#1124,.T.);
#2132=EDGE_CURVE('',#1749,#1760,#1125,.T.);
#2133=EDGE_CURVE('',#1743,#1761,#1126,.T.);
#2134=EDGE_CURVE('',#1762,#1761,#1127,.T.);
#2135=EDGE_CURVE('',#1763,#1762,#308,.T.);
#2136=EDGE_CURVE('',#1764,#1763,#1128,.T.);
#2137=EDGE_CURVE('',#1764,#1765,#1129,.T.);
#2138=EDGE_CURVE('',#1765,#1766,#1130,.T.);
#2139=EDGE_CURVE('',#1766,#1744,#1131,.T.);
#2140=EDGE_CURVE('',#1767,#1768,#1132,.T.);
#2141=EDGE_CURVE('',#1769,#1767,#1133,.T.);
#2142=EDGE_CURVE('',#1770,#1769,#1134,.T.);
#2143=EDGE_CURVE('',#1770,#1768,#1135,.T.);
#2144=EDGE_CURVE('',#1771,#1772,#1136,.T.);
#2145=EDGE_CURVE('',#1771,#1773,#1137,.T.);
#2146=EDGE_CURVE('',#1774,#1773,#1138,.T.);
#2147=EDGE_CURVE('',#1772,#1774,#1139,.T.);
#2148=EDGE_CURVE('',#1772,#1767,#1140,.T.);
#2149=EDGE_CURVE('',#1769,#1774,#1141,.T.);
#2150=EDGE_CURVE('',#1775,#1776,#1533,.T.);
#2151=EDGE_CURVE('',#1776,#1775,#1534,.T.);
#2152=EDGE_CURVE('',#1755,#1775,#1142,.T.);
#2153=EDGE_CURVE('',#1760,#1755,#1535,.T.);
#2154=EDGE_CURVE('',#1776,#1760,#1143,.T.);
#2155=EDGE_CURVE('',#1775,#1776,#309,.T.);
#2156=EDGE_CURVE('',#1777,#1752,#1144,.T.);
#2157=EDGE_CURVE('',#1777,#1770,#1145,.T.);
#2158=EDGE_CURVE('',#1773,#1778,#1146,.T.);
#2159=EDGE_CURVE('',#1778,#1775,#1147,.T.);
#2160=EDGE_CURVE('',#1751,#1776,#1148,.T.);
#2161=EDGE_CURVE('',#1778,#1756,#1149,.T.);
#2162=EDGE_CURVE('',#1758,#1752,#1150,.T.);
#2163=EDGE_CURVE('',#1757,#1777,#1151,.T.);
#2164=EDGE_CURVE('',#1751,#1759,#1152,.T.);
#2165=EDGE_CURVE('',#1759,#1758,#1536,.T.);
#2166=EDGE_CURVE('',#1758,#1759,#1537,.T.);
#2167=EDGE_CURVE('',#1779,#1754,#1153,.T.);
#2168=EDGE_CURVE('',#1779,#1780,#310,.T.);
#2169=EDGE_CURVE('',#1781,#1780,#1154,.T.);
#2170=EDGE_CURVE('',#1781,#1771,#1155,.T.);
#2171=EDGE_CURVE('',#1768,#1782,#1156,.T.);
#2172=EDGE_CURVE('',#1782,#1753,#1157,.T.);
#2173=EDGE_CURVE('',#1779,#1780,#1538,.T.);
#2174=EDGE_CURVE('',#1780,#1779,#1539,.T.);
#2175=EDGE_CURVE('',#1780,#1766,#1158,.T.);
#2176=EDGE_CURVE('',#1761,#1779,#1159,.T.);
#2177=EDGE_CURVE('',#1761,#1766,#1540,.T.);
#2178=EDGE_CURVE('',#1765,#1781,#1160,.T.);
#2179=EDGE_CURVE('',#1753,#1763,#1161,.T.);
#2180=EDGE_CURVE('',#1782,#1764,#1162,.T.);
#2181=EDGE_CURVE('',#1762,#1754,#1163,.T.);
#2182=EDGE_CURVE('',#1762,#1763,#1541,.T.);
#2183=EDGE_CURVE('',#1763,#1762,#1542,.T.);
#2799=ORIENTED_EDGE('',*,*,#2100,.F.);
#2800=ORIENTED_EDGE('',*,*,#2101,.T.);
#2801=ORIENTED_EDGE('',*,*,#2102,.F.);
#2802=ORIENTED_EDGE('',*,*,#2103,.F.);
#2803=ORIENTED_EDGE('',*,*,#2104,.F.);
#2804=ORIENTED_EDGE('',*,*,#2101,.F.);
#2805=ORIENTED_EDGE('',*,*,#2105,.F.);
#2806=ORIENTED_EDGE('',*,*,#2106,.F.);
#2807=ORIENTED_EDGE('',*,*,#2107,.T.);
#2808=ORIENTED_EDGE('',*,*,#2108,.F.);
#2809=ORIENTED_EDGE('',*,*,#2107,.F.);
#2810=ORIENTED_EDGE('',*,*,#2109,.F.);
#2811=ORIENTED_EDGE('',*,*,#2110,.F.);
#2812=ORIENTED_EDGE('',*,*,#2111,.F.);
#2813=ORIENTED_EDGE('',*,*,#2112,.T.);
#2814=ORIENTED_EDGE('',*,*,#2113,.F.);
#2815=ORIENTED_EDGE('',*,*,#2112,.F.);
#2816=ORIENTED_EDGE('',*,*,#2114,.F.);
#2817=ORIENTED_EDGE('',*,*,#2115,.F.);
#2818=ORIENTED_EDGE('',*,*,#2116,.T.);
#2819=ORIENTED_EDGE('',*,*,#2117,.F.);
#2820=ORIENTED_EDGE('',*,*,#2118,.F.);
#2821=ORIENTED_EDGE('',*,*,#2119,.F.);
#2822=ORIENTED_EDGE('',*,*,#2116,.F.);
#2823=ORIENTED_EDGE('',*,*,#2109,.T.);
#2824=ORIENTED_EDGE('',*,*,#2106,.T.);
#2825=ORIENTED_EDGE('',*,*,#2120,.T.);
#2826=ORIENTED_EDGE('',*,*,#2121,.F.);
#2827=ORIENTED_EDGE('',*,*,#2122,.T.);
#2828=ORIENTED_EDGE('',*,*,#2102,.T.);
#2829=ORIENTED_EDGE('',*,*,#2104,.T.);
#2830=ORIENTED_EDGE('',*,*,#2123,.T.);
#2831=ORIENTED_EDGE('',*,*,#2124,.T.);
#2832=ORIENTED_EDGE('',*,*,#2125,.T.);
#2833=ORIENTED_EDGE('',*,*,#2117,.T.);
#2834=ORIENTED_EDGE('',*,*,#2119,.T.);
#2835=ORIENTED_EDGE('',*,*,#2126,.F.);
#2836=ORIENTED_EDGE('',*,*,#2127,.F.);
#2837=ORIENTED_EDGE('',*,*,#2128,.T.);
#2838=ORIENTED_EDGE('',*,*,#2129,.T.);
#2839=ORIENTED_EDGE('',*,*,#2130,.F.);
#2840=ORIENTED_EDGE('',*,*,#2131,.F.);
#2841=ORIENTED_EDGE('',*,*,#2132,.F.);
#2842=ORIENTED_EDGE('',*,*,#2114,.T.);
#2843=ORIENTED_EDGE('',*,*,#2111,.T.);
#2844=ORIENTED_EDGE('',*,*,#2133,.T.);
#2845=ORIENTED_EDGE('',*,*,#2134,.F.);
#2846=ORIENTED_EDGE('',*,*,#2135,.F.);
#2847=ORIENTED_EDGE('',*,*,#2136,.F.);
#2848=ORIENTED_EDGE('',*,*,#2137,.T.);
#2849=ORIENTED_EDGE('',*,*,#2138,.T.);
#2850=ORIENTED_EDGE('',*,*,#2139,.T.);
#2851=ORIENTED_EDGE('',*,*,#2140,.F.);
#2852=ORIENTED_EDGE('',*,*,#2141,.F.);
#2853=ORIENTED_EDGE('',*,*,#2142,.F.);
#2854=ORIENTED_EDGE('',*,*,#2143,.T.);
#2855=ORIENTED_EDGE('',*,*,#2144,.F.);
#2856=ORIENTED_EDGE('',*,*,#2145,.T.);
#2857=ORIENTED_EDGE('',*,*,#2146,.F.);
#2858=ORIENTED_EDGE('',*,*,#2147,.F.);
#2859=ORIENTED_EDGE('',*,*,#2148,.F.);
#2860=ORIENTED_EDGE('',*,*,#2147,.T.);
#2861=ORIENTED_EDGE('',*,*,#2149,.F.);
#2862=ORIENTED_EDGE('',*,*,#2141,.T.);
#2863=ORIENTED_EDGE('',*,*,#2150,.F.);
#2864=ORIENTED_EDGE('',*,*,#2151,.F.);
#2865=ORIENTED_EDGE('',*,*,#2115,.T.);
#2866=ORIENTED_EDGE('',*,*,#2152,.F.);
#2867=ORIENTED_EDGE('',*,*,#2153,.F.);
#2868=ORIENTED_EDGE('',*,*,#2154,.F.);
#2869=ORIENTED_EDGE('',*,*,#2151,.T.);
#2870=ORIENTED_EDGE('',*,*,#2118,.T.);
#2871=ORIENTED_EDGE('',*,*,#2132,.T.);
#2872=ORIENTED_EDGE('',*,*,#2153,.T.);
#2873=ORIENTED_EDGE('',*,*,#2126,.T.);
#2874=ORIENTED_EDGE('',*,*,#2155,.F.);
#2875=ORIENTED_EDGE('',*,*,#2150,.T.);
#2876=ORIENTED_EDGE('',*,*,#2105,.T.);
#2877=ORIENTED_EDGE('',*,*,#2122,.F.);
#2878=ORIENTED_EDGE('',*,*,#2156,.F.);
#2879=ORIENTED_EDGE('',*,*,#2157,.T.);
#2880=ORIENTED_EDGE('',*,*,#2142,.T.);
#2881=ORIENTED_EDGE('',*,*,#2149,.T.);
#2882=ORIENTED_EDGE('',*,*,#2146,.T.);
#2883=ORIENTED_EDGE('',*,*,#2158,.T.);
#2884=ORIENTED_EDGE('',*,*,#2159,.T.);
#2885=ORIENTED_EDGE('',*,*,#2155,.T.);
#2886=ORIENTED_EDGE('',*,*,#2160,.F.);
#2887=ORIENTED_EDGE('',*,*,#2120,.F.);
#2888=ORIENTED_EDGE('',*,*,#2152,.T.);
#2889=ORIENTED_EDGE('',*,*,#2159,.F.);
#2890=ORIENTED_EDGE('',*,*,#2161,.T.);
#2891=ORIENTED_EDGE('',*,*,#2127,.T.);
#2892=ORIENTED_EDGE('',*,*,#2162,.F.);
#2893=ORIENTED_EDGE('',*,*,#2129,.F.);
#2894=ORIENTED_EDGE('',*,*,#2163,.T.);
#2895=ORIENTED_EDGE('',*,*,#2156,.T.);
#2896=ORIENTED_EDGE('',*,*,#2164,.F.);
#2897=ORIENTED_EDGE('',*,*,#2160,.T.);
#2898=ORIENTED_EDGE('',*,*,#2154,.T.);
#2899=ORIENTED_EDGE('',*,*,#2131,.T.);
#2900=ORIENTED_EDGE('',*,*,#2130,.T.);
#2901=ORIENTED_EDGE('',*,*,#2165,.F.);
#2902=ORIENTED_EDGE('',*,*,#2164,.T.);
#2903=ORIENTED_EDGE('',*,*,#2166,.F.);
#2904=ORIENTED_EDGE('',*,*,#2162,.T.);
#2905=ORIENTED_EDGE('',*,*,#2121,.T.);
#2906=ORIENTED_EDGE('',*,*,#2165,.T.);
#2907=ORIENTED_EDGE('',*,*,#2166,.T.);
#2908=ORIENTED_EDGE('',*,*,#2108,.T.);
#2909=ORIENTED_EDGE('',*,*,#2103,.T.);
#2910=ORIENTED_EDGE('',*,*,#2125,.F.);
#2911=ORIENTED_EDGE('',*,*,#2167,.F.);
#2912=ORIENTED_EDGE('',*,*,#2168,.T.);
#2913=ORIENTED_EDGE('',*,*,#2169,.F.);
#2914=ORIENTED_EDGE('',*,*,#2170,.T.);
#2915=ORIENTED_EDGE('',*,*,#2144,.T.);
#2916=ORIENTED_EDGE('',*,*,#2148,.T.);
#2917=ORIENTED_EDGE('',*,*,#2140,.T.);
#2918=ORIENTED_EDGE('',*,*,#2171,.T.);
#2919=ORIENTED_EDGE('',*,*,#2172,.T.);
#2920=ORIENTED_EDGE('',*,*,#2123,.F.);
#2921=ORIENTED_EDGE('',*,*,#2173,.T.);
#2922=ORIENTED_EDGE('',*,*,#2174,.T.);
#2923=ORIENTED_EDGE('',*,*,#2113,.T.);
#2924=ORIENTED_EDGE('',*,*,#2168,.F.);
#2925=ORIENTED_EDGE('',*,*,#2174,.F.);
#2926=ORIENTED_EDGE('',*,*,#2175,.F.);
#2927=ORIENTED_EDGE('',*,*,#2173,.F.);
#2928=ORIENTED_EDGE('',*,*,#2176,.F.);
#2929=ORIENTED_EDGE('',*,*,#2177,.T.);
#2930=ORIENTED_EDGE('',*,*,#2110,.T.);
#2931=ORIENTED_EDGE('',*,*,#2139,.F.);
#2932=ORIENTED_EDGE('',*,*,#2177,.F.);
#2933=ORIENTED_EDGE('',*,*,#2133,.F.);
#2934=ORIENTED_EDGE('',*,*,#2175,.T.);
#2935=ORIENTED_EDGE('',*,*,#2138,.F.);
#2936=ORIENTED_EDGE('',*,*,#2178,.T.);
#2937=ORIENTED_EDGE('',*,*,#2169,.T.);
#2938=ORIENTED_EDGE('',*,*,#2179,.F.);
#2939=ORIENTED_EDGE('',*,*,#2172,.F.);
#2940=ORIENTED_EDGE('',*,*,#2180,.T.);
#2941=ORIENTED_EDGE('',*,*,#2136,.T.);
#2942=ORIENTED_EDGE('',*,*,#2181,.F.);
#2943=ORIENTED_EDGE('',*,*,#2134,.T.);
#2944=ORIENTED_EDGE('',*,*,#2176,.T.);
#2945=ORIENTED_EDGE('',*,*,#2167,.T.);
#2946=ORIENTED_EDGE('',*,*,#2170,.F.);
#2947=ORIENTED_EDGE('',*,*,#2178,.F.);
#2948=ORIENTED_EDGE('',*,*,#2137,.F.);
#2949=ORIENTED_EDGE('',*,*,#2180,.F.);
#2950=ORIENTED_EDGE('',*,*,#2171,.F.);
#2951=ORIENTED_EDGE('',*,*,#2143,.F.);
#2952=ORIENTED_EDGE('',*,*,#2157,.F.);
#2953=ORIENTED_EDGE('',*,*,#2163,.F.);
#2954=ORIENTED_EDGE('',*,*,#2128,.F.);
#2955=ORIENTED_EDGE('',*,*,#2161,.F.);
#2956=ORIENTED_EDGE('',*,*,#2158,.F.);
#2957=ORIENTED_EDGE('',*,*,#2145,.F.);
#2958=ORIENTED_EDGE('',*,*,#2182,.F.);
#2959=ORIENTED_EDGE('',*,*,#2183,.F.);
#2960=ORIENTED_EDGE('',*,*,#2100,.T.);
#2961=ORIENTED_EDGE('',*,*,#2135,.T.);
#2962=ORIENTED_EDGE('',*,*,#2182,.T.);
#2963=ORIENTED_EDGE('',*,*,#2179,.T.);
#2964=ORIENTED_EDGE('',*,*,#2183,.T.);
#2965=ORIENTED_EDGE('',*,*,#2181,.T.);
#2966=ORIENTED_EDGE('',*,*,#2124,.F.);
#3130=CYLINDRICAL_SURFACE('',#3641,0.41);
#3131=CYLINDRICAL_SURFACE('',#3646,0.41);
#3132=CYLINDRICAL_SURFACE('',#3651,0.41);
#3133=CYLINDRICAL_SURFACE('',#3656,0.41);
#3134=CYLINDRICAL_SURFACE('',#3675,0.7);
#3135=CYLINDRICAL_SURFACE('',#3678,0.7);
#3136=CYLINDRICAL_SURFACE('',#3684,0.7);
#3137=CYLINDRICAL_SURFACE('',#3686,0.7);
#3138=CYLINDRICAL_SURFACE('',#3694,0.7);
#3139=CYLINDRICAL_SURFACE('',#3695,0.7);
#3140=CYLINDRICAL_SURFACE('',#3705,0.7);
#3141=CYLINDRICAL_SURFACE('',#3706,0.7);
#3264=ADVANCED_FACE('',(#642),#3130,.F.);
#3265=ADVANCED_FACE('',(#643),#3131,.F.);
#3266=ADVANCED_FACE('',(#644),#3132,.F.);
#3267=ADVANCED_FACE('',(#645),#3133,.F.);
#3268=ADVANCED_FACE('',(#646),#483,.F.);
#3269=ADVANCED_FACE('',(#647),#484,.T.);
#3270=ADVANCED_FACE('',(#648),#485,.T.);
#3271=ADVANCED_FACE('',(#649),#486,.T.);
#3272=ADVANCED_FACE('',(#650),#487,.T.);
#3273=ADVANCED_FACE('',(#651),#488,.T.);
#3274=ADVANCED_FACE('',(#652),#489,.T.);
#3275=ADVANCED_FACE('',(#653,#393),#490,.F.);
#3276=ADVANCED_FACE('',(#654),#3134,.T.);
#3277=ADVANCED_FACE('',(#655),#491,.T.);
#3278=ADVANCED_FACE('',(#656),#3135,.T.);
#3279=ADVANCED_FACE('',(#657),#492,.T.);
#3280=ADVANCED_FACE('',(#658),#493,.T.);
#3281=ADVANCED_FACE('',(#659),#494,.T.);
#3282=ADVANCED_FACE('',(#660),#495,.T.);
#3283=ADVANCED_FACE('',(#661),#3136,.T.);
#3284=ADVANCED_FACE('',(#662),#3137,.T.);
#3285=ADVANCED_FACE('',(#663,#394),#496,.T.);
#3286=ADVANCED_FACE('',(#664),#497,.T.);
#3287=ADVANCED_FACE('',(#665,#395),#498,.T.);
#3288=ADVANCED_FACE('',(#666),#3138,.T.);
#3289=ADVANCED_FACE('',(#667),#3139,.T.);
#3290=ADVANCED_FACE('',(#668),#499,.F.);
#3291=ADVANCED_FACE('',(#669),#500,.T.);
#3292=ADVANCED_FACE('',(#670),#501,.T.);
#3293=ADVANCED_FACE('',(#671),#502,.T.);
#3294=ADVANCED_FACE('',(#672),#503,.F.);
#3295=ADVANCED_FACE('',(#673,#396),#504,.F.);
#3296=ADVANCED_FACE('',(#674),#3140,.T.);
#3297=ADVANCED_FACE('',(#675),#3141,.T.);
#3339=CLOSED_SHELL('',(#3264,#3265,#3266,#3267,#3268,#3269,#3270,#3271,
#3272,#3273,#3274,#3275,#3276,#3277,#3278,#3279,#3280,#3281,#3282,#3283,
#3284,#3285,#3286,#3287,#3288,#3289,#3290,#3291,#3292,#3293,#3294,#3295,
#3296,#3297));
#3640=AXIS2_PLACEMENT_3D('',#5483,#4429,#4430);
#3641=AXIS2_PLACEMENT_3D('',#5484,#4431,#4432);
#3642=AXIS2_PLACEMENT_3D('',#5486,#4433,#4434);
#3643=AXIS2_PLACEMENT_3D('',#5490,#4436,#4437);
#3644=AXIS2_PLACEMENT_3D('',#5492,#4438,#4439);
#3645=AXIS2_PLACEMENT_3D('',#5493,#4440,#4441);
#3646=AXIS2_PLACEMENT_3D('',#5494,#4442,#4443);
#3647=AXIS2_PLACEMENT_3D('',#5497,#4444,#4445);
#3648=AXIS2_PLACEMENT_3D('',#5499,#4446,#4447);
#3649=AXIS2_PLACEMENT_3D('',#5502,#4449,#4450);
#3650=AXIS2_PLACEMENT_3D('',#5503,#4451,#4452);
#3651=AXIS2_PLACEMENT_3D('',#5504,#4453,#4454);
#3652=AXIS2_PLACEMENT_3D('',#5507,#4455,#4456);
#3653=AXIS2_PLACEMENT_3D('',#5509,#4457,#4458);
#3654=AXIS2_PLACEMENT_3D('',#5512,#4460,#4461);
#3655=AXIS2_PLACEMENT_3D('',#5513,#4462,#4463);
#3656=AXIS2_PLACEMENT_3D('',#5514,#4464,#4465);
#3657=AXIS2_PLACEMENT_3D('',#5516,#4466,#4467);
#3658=AXIS2_PLACEMENT_3D('',#5520,#4469,#4470);
#3659=AXIS2_PLACEMENT_3D('',#5522,#4471,#4472);
#3660=AXIS2_PLACEMENT_3D('',#5523,#4473,#4474);
#3661=AXIS2_PLACEMENT_3D('',#5524,#4475,#4476);
#3662=AXIS2_PLACEMENT_3D('',#5528,#4478,#4479);
#3663=AXIS2_PLACEMENT_3D('',#5530,#4481,#4482);
#3664=AXIS2_PLACEMENT_3D('',#5534,#4484,#4485);
#3665=AXIS2_PLACEMENT_3D('',#5536,#4487,#4488);
#3666=AXIS2_PLACEMENT_3D('',#5546,#4493,#4494);
#3667=AXIS2_PLACEMENT_3D('',#5550,#4497,#4498);
#3668=AXIS2_PLACEMENT_3D('',#5556,#4501,#4502);
#3669=AXIS2_PLACEMENT_3D('',#5564,#4507,#4508);
#3670=AXIS2_PLACEMENT_3D('',#5573,#4513,#4514);
#3671=AXIS2_PLACEMENT_3D('',#5582,#4519,#4520);
#3672=AXIS2_PLACEMENT_3D('',#5585,#4523,#4524);
#3673=AXIS2_PLACEMENT_3D('',#5588,#4525,#4526);
#3674=AXIS2_PLACEMENT_3D('',#5589,#4527,#4528);
#3675=AXIS2_PLACEMENT_3D('',#5590,#4529,#4530);
#3676=AXIS2_PLACEMENT_3D('',#5592,#4532,#4533);
#3677=AXIS2_PLACEMENT_3D('',#5594,#4535,#4536);
#3678=AXIS2_PLACEMENT_3D('',#5595,#4537,#4538);
#3679=AXIS2_PLACEMENT_3D('',#5596,#4539,#4540);
#3680=AXIS2_PLACEMENT_3D('',#5597,#4541,#4542);
#3681=AXIS2_PLACEMENT_3D('',#5605,#4548,#4549);
#3682=AXIS2_PLACEMENT_3D('',#5607,#4551,#4552);
#3683=AXIS2_PLACEMENT_3D('',#5610,#4555,#4556);
#3684=AXIS2_PLACEMENT_3D('',#5612,#4558,#4559);
#3685=AXIS2_PLACEMENT_3D('',#5613,#4560,#4561);
#3686=AXIS2_PLACEMENT_3D('',#5614,#4562,#4563);
#3687=AXIS2_PLACEMENT_3D('',#5615,#4564,#4565);
#3688=AXIS2_PLACEMENT_3D('',#5616,#4566,#4567);
#3689=AXIS2_PLACEMENT_3D('',#5617,#4568,#4569);
#3690=AXIS2_PLACEMENT_3D('',#5621,#4571,#4572);
#3691=AXIS2_PLACEMENT_3D('',#5628,#4577,#4578);
#3692=AXIS2_PLACEMENT_3D('',#5629,#4579,#4580);
#3693=AXIS2_PLACEMENT_3D('',#5630,#4581,#4582);
#3694=AXIS2_PLACEMENT_3D('',#5631,#4583,#4584);
#3695=AXIS2_PLACEMENT_3D('',#5632,#4585,#4586);
#3696=AXIS2_PLACEMENT_3D('',#5635,#4589,#4590);
#3697=AXIS2_PLACEMENT_3D('',#5636,#4591,#4592);
#3698=AXIS2_PLACEMENT_3D('',#5637,#4593,#4594);
#3699=AXIS2_PLACEMENT_3D('',#5639,#4596,#4597);
#3700=AXIS2_PLACEMENT_3D('',#5642,#4600,#4601);
#3701=AXIS2_PLACEMENT_3D('',#5644,#4603,#4604);
#3702=AXIS2_PLACEMENT_3D('',#5645,#4605,#4606);
#3703=AXIS2_PLACEMENT_3D('',#5646,#4607,#4608);
#3704=AXIS2_PLACEMENT_3D('',#5647,#4609,#4610);
#3705=AXIS2_PLACEMENT_3D('',#5648,#4611,#4612);
#3706=AXIS2_PLACEMENT_3D('',#5649,#4613,#4614);
#4429=DIRECTION('axis',(0.,0.,1.));
#4430=DIRECTION('refdir',(1.,0.,0.));
#4431=DIRECTION('center_axis',(0.,1.,0.));
#4432=DIRECTION('ref_axis',(1.,0.,0.));
#4433=DIRECTION('center_axis',(0.,1.,0.));
#4434=DIRECTION('ref_axis',(1.,0.,0.));
#4435=DIRECTION('',(0.,1.,0.));
#4436=DIRECTION('center_axis',(0.,-1.,0.));
#4437=DIRECTION('ref_axis',(1.,0.,0.));
#4438=DIRECTION('center_axis',(0.157990501106673,-0.987440631916705,0.));
#4439=DIRECTION('ref_axis',(0.987440631916705,0.157990501106673,0.));
#4440=DIRECTION('center_axis',(0.,-1.,0.));
#4441=DIRECTION('ref_axis',(1.,0.,0.));
#4442=DIRECTION('center_axis',(0.,1.,0.));
#4443=DIRECTION('ref_axis',(1.,0.,0.));
#4444=DIRECTION('center_axis',(0.157990501106673,0.987440631916705,0.));
#4445=DIRECTION('ref_axis',(0.987440631916705,-0.157990501106673,0.));
#4446=DIRECTION('center_axis',(0.,1.,0.));
#4447=DIRECTION('ref_axis',(1.,0.,0.));
#4448=DIRECTION('',(0.,1.,0.));
#4449=DIRECTION('center_axis',(0.,-1.,0.));
#4450=DIRECTION('ref_axis',(1.,0.,0.));
#4451=DIRECTION('center_axis',(0.,1.,0.));
#4452=DIRECTION('ref_axis',(1.,0.,0.));
#4453=DIRECTION('center_axis',(0.,1.,0.));
#4454=DIRECTION('ref_axis',(1.,0.,0.));
#4455=DIRECTION('center_axis',(0.,1.,0.));
#4456=DIRECTION('ref_axis',(1.,0.,0.));
#4457=DIRECTION('center_axis',(-0.157990501106673,0.987440631916705,0.));
#4458=DIRECTION('ref_axis',(0.987440631916705,0.157990501106673,0.));
#4459=DIRECTION('',(0.,1.,0.));
#4460=DIRECTION('center_axis',(0.,-1.,0.));
#4461=DIRECTION('ref_axis',(1.,0.,0.));
#4462=DIRECTION('center_axis',(-0.157990501106673,0.987440631916705,0.));
#4463=DIRECTION('ref_axis',(0.987440631916705,0.157990501106673,0.));
#4464=DIRECTION('center_axis',(0.,1.,0.));
#4465=DIRECTION('ref_axis',(1.,0.,0.));
#4466=DIRECTION('center_axis',(0.,1.,0.));
#4467=DIRECTION('ref_axis',(1.,0.,0.));
#4468=DIRECTION('',(0.,1.,0.));
#4469=DIRECTION('center_axis',(-0.157990501106673,-0.987440631916705,0.));
#4470=DIRECTION('ref_axis',(0.987440631916705,-0.157990501106673,0.));
#4471=DIRECTION('center_axis',(0.,-1.,0.));
#4472=DIRECTION('ref_axis',(1.,0.,0.));
#4473=DIRECTION('center_axis',(-0.157990501106673,-0.987440631916705,0.));
#4474=DIRECTION('ref_axis',(0.987440631916705,-0.157990501106673,0.));
#4475=DIRECTION('center_axis',(0.,1.,0.));
#4476=DIRECTION('ref_axis',(1.,0.,0.));
#4477=DIRECTION('',(0.,0.,1.));
#4478=DIRECTION('center_axis',(0.,1.,0.));
#4479=DIRECTION('ref_axis',(1.,0.,0.));
#4480=DIRECTION('',(0.,0.,1.));
#4481=DIRECTION('center_axis',(0.,1.,0.));
#4482=DIRECTION('ref_axis',(1.,0.,0.));
#4483=DIRECTION('',(0.,0.,-1.));
#4484=DIRECTION('center_axis',(0.,1.,0.));
#4485=DIRECTION('ref_axis',(1.,0.,0.));
#4486=DIRECTION('',(0.,0.,-1.));
#4487=DIRECTION('center_axis',(0.157990501106673,0.987440631916705,0.));
#4488=DIRECTION('ref_axis',(-0.987440631916705,0.157990501106673,0.));
#4489=DIRECTION('',(0.,0.,1.));
#4490=DIRECTION('',(0.,0.,1.));
#4491=DIRECTION('',(-0.987440631916705,0.157990501106673,0.));
#4492=DIRECTION('',(0.,0.,1.));
#4493=DIRECTION('center_axis',(0.157990501106673,0.987440631916705,0.));
#4494=DIRECTION('ref_axis',(0.987440631916705,-0.157990501106673,0.));
#4495=DIRECTION('',(-0.987440631916705,0.157990501106673,0.));
#4496=DIRECTION('',(0.,0.,1.));
#4497=DIRECTION('center_axis',(0.157990501106673,-0.987440631916705,0.));
#4498=DIRECTION('ref_axis',(0.987440631916705,0.157990501106673,0.));
#4499=DIRECTION('',(0.,0.,1.));
#4500=DIRECTION('',(0.987440631916705,0.157990501106673,0.));
#4501=DIRECTION('center_axis',(0.157990501106673,-0.987440631916705,0.));
#4502=DIRECTION('ref_axis',(0.987440631916705,0.157990501106673,0.));
#4503=DIRECTION('',(0.,0.,1.));
#4504=DIRECTION('',(0.987440631916705,0.157990501106673,0.));
#4505=DIRECTION('',(0.,0.,1.));
#4506=DIRECTION('',(0.,0.,1.));
#4507=DIRECTION('center_axis',(-1.,0.,0.));
#4508=DIRECTION('ref_axis',(0.,-1.,0.));
#4509=DIRECTION('',(0.,0.,-1.));
#4510=DIRECTION('',(0.,-1.,0.));
#4511=DIRECTION('',(0.,0.,1.));
#4512=DIRECTION('',(0.,-1.,0.));
#4513=DIRECTION('center_axis',(1.,0.,0.));
#4514=DIRECTION('ref_axis',(0.,1.,0.));
#4515=DIRECTION('',(0.,0.,1.));
#4516=DIRECTION('',(0.,1.,0.));
#4517=DIRECTION('',(0.,0.,-1.));
#4518=DIRECTION('',(0.,1.,0.));
#4519=DIRECTION('center_axis',(0.,0.,1.));
#4520=DIRECTION('ref_axis',(1.,0.,0.));
#4521=DIRECTION('',(-0.987440631916705,-0.157990501106673,0.));
#4522=DIRECTION('',(0.987440631916705,-0.157990501106673,0.));
#4523=DIRECTION('center_axis',(0.,1.,0.));
#4524=DIRECTION('ref_axis',(1.,0.,0.));
#4525=DIRECTION('center_axis',(0.,1.,0.));
#4526=DIRECTION('ref_axis',(1.,0.,0.));
#4527=DIRECTION('center_axis',(0.,1.,0.));
#4528=DIRECTION('ref_axis',(1.,0.,0.));
#4529=DIRECTION('center_axis',(0.,1.,0.));
#4530=DIRECTION('ref_axis',(1.,0.,0.));
#4531=DIRECTION('',(0.,-1.,0.));
#4532=DIRECTION('center_axis',(0.,1.,0.));
#4533=DIRECTION('ref_axis',(1.,0.,0.));
#4534=DIRECTION('',(0.,1.,0.));
#4535=DIRECTION('center_axis',(0.,1.,0.));
#4536=DIRECTION('ref_axis',(1.,0.,0.));
#4537=DIRECTION('center_axis',(0.,1.,0.));
#4538=DIRECTION('ref_axis',(-1.,0.,1.22464679914735E-16));
#4539=DIRECTION('center_axis',(0.157990501106673,0.987440631916705,0.));
#4540=DIRECTION('ref_axis',(0.987440631916706,-0.157990501106673,0.));
#4541=DIRECTION('center_axis',(-0.157990501106673,-0.987440631916705,0.));
#4542=DIRECTION('ref_axis',(0.987440631916705,-0.157990501106673,0.));
#4543=DIRECTION('',(0.,0.,1.));
#4544=DIRECTION('',(0.987440631916705,-0.157990501106673,0.));
#4545=DIRECTION('',(0.987440631916705,-0.157990501106673,0.));
#4546=DIRECTION('',(0.,0.,1.));
#4547=DIRECTION('',(0.987440631916705,-0.157990501106673,0.));
#4548=DIRECTION('center_axis',(1.,0.,0.));
#4549=DIRECTION('ref_axis',(0.,1.,0.));
#4550=DIRECTION('',(0.,1.,0.));
#4551=DIRECTION('center_axis',(-1.,0.,0.));
#4552=DIRECTION('ref_axis',(0.,-1.,0.));
#4553=DIRECTION('',(0.,-1.,0.));
#4554=DIRECTION('',(0.,-1.,0.));
#4555=DIRECTION('center_axis',(0.,0.,1.));
#4556=DIRECTION('ref_axis',(1.,0.,0.));
#4557=DIRECTION('',(0.,1.,0.));
#4558=DIRECTION('center_axis',(0.,1.,0.));
#4559=DIRECTION('ref_axis',(1.,0.,0.));
#4560=DIRECTION('center_axis',(0.,1.,0.));
#4561=DIRECTION('ref_axis',(1.,0.,0.));
#4562=DIRECTION('center_axis',(0.,1.,0.));
#4563=DIRECTION('ref_axis',(-1.,0.,1.22464679914735E-16));
#4564=DIRECTION('center_axis',(0.,1.,0.));
#4565=DIRECTION('ref_axis',(1.,0.,0.));
#4566=DIRECTION('center_axis',(0.,1.,0.));
#4567=DIRECTION('ref_axis',(1.,0.,0.));
#4568=DIRECTION('center_axis',(-0.157990501106673,0.987440631916705,0.));
#4569=DIRECTION('ref_axis',(-0.987440631916705,-0.157990501106673,0.));
#4570=DIRECTION('',(-0.987440631916705,-0.157990501106673,0.));
#4571=DIRECTION('center_axis',(0.157990501106673,-0.987440631916705,0.));
#4572=DIRECTION('ref_axis',(0.987440631916706,0.157990501106673,0.));
#4573=DIRECTION('',(0.,0.,1.));
#4574=DIRECTION('',(-0.987440631916705,-0.157990501106673,0.));
#4575=DIRECTION('',(-0.987440631916705,-0.157990501106673,0.));
#4576=DIRECTION('',(0.,0.,1.));
#4577=DIRECTION('center_axis',(0.,1.,0.));
#4578=DIRECTION('ref_axis',(1.,0.,0.));
#4579=DIRECTION('center_axis',(0.,1.,0.));
#4580=DIRECTION('ref_axis',(1.,0.,0.));
#4581=DIRECTION('center_axis',(0.,1.,0.));
#4582=DIRECTION('ref_axis',(1.,0.,0.));
#4583=DIRECTION('center_axis',(0.,1.,0.));
#4584=DIRECTION('ref_axis',(-1.,0.,-1.01064309961486E-15));
#4585=DIRECTION('center_axis',(0.,1.,0.));
#4586=DIRECTION('ref_axis',(1.,0.,0.));
#4587=DIRECTION('',(0.,-1.,0.));
#4588=DIRECTION('',(0.,1.,0.));
#4589=DIRECTION('center_axis',(0.,1.,0.));
#4590=DIRECTION('ref_axis',(1.,0.,0.));
#4591=DIRECTION('center_axis',(0.,1.,0.));
#4592=DIRECTION('ref_axis',(1.,0.,0.));
#4593=DIRECTION('center_axis',(1.,0.,0.));
#4594=DIRECTION('ref_axis',(0.,1.,0.));
#4595=DIRECTION('',(0.,1.,0.));
#4596=DIRECTION('center_axis',(-1.,0.,0.));
#4597=DIRECTION('ref_axis',(0.,-1.,0.));
#4598=DIRECTION('',(0.,-1.,0.));
#4599=DIRECTION('',(0.,-1.,0.));
#4600=DIRECTION('center_axis',(0.,0.,1.));
#4601=DIRECTION('ref_axis',(1.,0.,0.));
#4602=DIRECTION('',(0.,1.,0.));
#4603=DIRECTION('center_axis',(0.,0.,1.));
#4604=DIRECTION('ref_axis',(1.,0.,0.));
#4605=DIRECTION('center_axis',(0.,1.,0.));
#4606=DIRECTION('ref_axis',(1.,0.,0.));
#4607=DIRECTION('center_axis',(0.,1.,0.));
#4608=DIRECTION('ref_axis',(1.,0.,0.));
#4609=DIRECTION('center_axis',(0.,1.,0.));
#4610=DIRECTION('ref_axis',(1.,0.,0.));
#4611=DIRECTION('center_axis',(0.,1.,0.));
#4612=DIRECTION('ref_axis',(1.,0.,0.));
#4613=DIRECTION('center_axis',(0.,1.,0.));
#4614=DIRECTION('ref_axis',(-1.,0.,-1.22464679914735E-16));
#5483=CARTESIAN_POINT('',(0.,0.,0.));
#5484=CARTESIAN_POINT('Origin',(0.,-1.7,3.));
#5485=CARTESIAN_POINT('',(-0.41,-1.52,3.));
#5486=CARTESIAN_POINT('Origin',(0.,-1.52,3.));
#5487=CARTESIAN_POINT('',(-0.41,-1.28,3.));
#5488=CARTESIAN_POINT('',(-0.41,-1.7,3.));
#5489=CARTESIAN_POINT('',(2.22044604925031E-16,-1.28,3.41));
#5490=CARTESIAN_POINT('Origin',(0.,-1.28,3.));
#5491=CARTESIAN_POINT('',(2.22044604925031E-16,-1.28,2.59));
#5492=CARTESIAN_POINT('Origin',(0.,-1.28,3.));
#5493=CARTESIAN_POINT('Origin',(0.,-1.28,3.));
#5494=CARTESIAN_POINT('Origin',(0.,-1.7,3.));
#5495=CARTESIAN_POINT('',(-1.73201719910321E-17,1.28,3.41));
#5496=CARTESIAN_POINT('',(-1.73201719910321E-17,1.28,2.59));
#5497=CARTESIAN_POINT('Origin',(0.,1.28,3.));
#5498=CARTESIAN_POINT('',(-0.41,1.28,3.));
#5499=CARTESIAN_POINT('Origin',(0.,1.28,3.));
#5500=CARTESIAN_POINT('',(-0.41,1.52,3.));
#5501=CARTESIAN_POINT('',(-0.41,-1.7,3.));
#5502=CARTESIAN_POINT('Origin',(0.,1.52,3.));
#5503=CARTESIAN_POINT('Origin',(0.,1.28,3.));
#5504=CARTESIAN_POINT('Origin',(2.5,-1.7,3.));
#5505=CARTESIAN_POINT('',(2.5,-1.12,3.41));
#5506=CARTESIAN_POINT('',(2.5,-1.12,2.59));
#5507=CARTESIAN_POINT('Origin',(2.5,-1.12,3.));
#5508=CARTESIAN_POINT('',(2.09,-1.1856,3.));
#5509=CARTESIAN_POINT('Origin',(2.5,-1.12,3.));
#5510=CARTESIAN_POINT('',(2.09,-0.88,3.));
#5511=CARTESIAN_POINT('',(2.09,-1.7,3.));
#5512=CARTESIAN_POINT('Origin',(2.5,-0.88,3.));
#5513=CARTESIAN_POINT('Origin',(2.5,-1.12,3.));
#5514=CARTESIAN_POINT('Origin',(2.5,-1.7,3.));
#5515=CARTESIAN_POINT('',(2.09,0.88,3.));
#5516=CARTESIAN_POINT('Origin',(2.5,0.88,3.));
#5517=CARTESIAN_POINT('',(2.09,1.1856,3.));
#5518=CARTESIAN_POINT('',(2.09,-1.7,3.));
#5519=CARTESIAN_POINT('',(2.5,1.12,3.41));
#5520=CARTESIAN_POINT('Origin',(2.5,1.12,3.));
#5521=CARTESIAN_POINT('',(2.5,1.12,2.59));
#5522=CARTESIAN_POINT('Origin',(2.5,1.12,3.));
#5523=CARTESIAN_POINT('Origin',(2.5,1.12,3.));
#5524=CARTESIAN_POINT('Origin',(0.,1.28,3.));
#5525=CARTESIAN_POINT('',(0.,1.28,3.7));
#5526=CARTESIAN_POINT('',(-1.73201719910321E-17,1.28,2.));
#5527=CARTESIAN_POINT('',(0.,1.28,2.3));
#5528=CARTESIAN_POINT('Origin',(0.,1.28,3.));
#5529=CARTESIAN_POINT('',(-1.73201719910321E-17,1.28,2.));
#5530=CARTESIAN_POINT('Origin',(0.,-1.28,3.));
#5531=CARTESIAN_POINT('',(0.,-1.28,2.3));
#5532=CARTESIAN_POINT('',(2.22044604925031E-16,-1.28,2.));
#5533=CARTESIAN_POINT('',(0.,-1.28,3.7));
#5534=CARTESIAN_POINT('Origin',(0.,-1.28,3.));
#5535=CARTESIAN_POINT('',(2.22044604925031E-16,-1.28,2.));
#5536=CARTESIAN_POINT('Origin',(2.5,1.12,1.));
#5537=CARTESIAN_POINT('',(2.5,1.12,2.3));
#5538=CARTESIAN_POINT('',(2.5,1.12,1.));
#5539=CARTESIAN_POINT('',(2.5,1.12,1.));
#5540=CARTESIAN_POINT('',(2.5,1.12,1.));
#5541=CARTESIAN_POINT('',(0.,1.52,1.));
#5542=CARTESIAN_POINT('',(2.5,1.12,1.));
#5543=CARTESIAN_POINT('',(0.,1.52,2.3));
#5544=CARTESIAN_POINT('',(0.,1.52,1.));
#5545=CARTESIAN_POINT('',(0.,1.52,3.7));
#5546=CARTESIAN_POINT('Origin',(0.,1.52,3.));
#5547=CARTESIAN_POINT('',(2.5,1.12,3.7));
#5548=CARTESIAN_POINT('',(2.5,1.12,3.7));
#5549=CARTESIAN_POINT('',(2.5,1.12,1.));
#5550=CARTESIAN_POINT('Origin',(0.,-1.52,1.));
#5551=CARTESIAN_POINT('',(2.5,-1.12,3.7));
#5552=CARTESIAN_POINT('',(2.5,-1.12,1.));
#5553=CARTESIAN_POINT('',(0.,-1.52,3.7));
#5554=CARTESIAN_POINT('',(0.,-1.52,3.7));
#5555=CARTESIAN_POINT('',(0.,-1.52,2.3));
#5556=CARTESIAN_POINT('Origin',(0.,-1.52,3.));
#5557=CARTESIAN_POINT('',(0.,-1.52,1.));
#5558=CARTESIAN_POINT('',(0.,-1.52,1.));
#5559=CARTESIAN_POINT('',(2.5,-1.12,1.));
#5560=CARTESIAN_POINT('',(0.,-1.52,1.));
#5561=CARTESIAN_POINT('',(2.5,-1.12,2.3));
#5562=CARTESIAN_POINT('',(2.5,-1.12,1.));
#5563=CARTESIAN_POINT('',(2.5,-1.12,1.));
#5564=CARTESIAN_POINT('Origin',(0.8,1.3,1.));
#5565=CARTESIAN_POINT('',(0.8,-1.152,1.3));
#5566=CARTESIAN_POINT('',(0.8,-1.152,1.));
#5567=CARTESIAN_POINT('',(0.8,-1.152,1.));
#5568=CARTESIAN_POINT('',(0.8,1.152,1.3));
#5569=CARTESIAN_POINT('',(0.8,1.3,1.3));
#5570=CARTESIAN_POINT('',(0.8,1.152,1.));
#5571=CARTESIAN_POINT('',(0.8,1.152,1.));
#5572=CARTESIAN_POINT('',(0.8,1.3,1.));
#5573=CARTESIAN_POINT('Origin',(1.7,-1.15,1.));
#5574=CARTESIAN_POINT('',(1.7,-1.008,1.));
#5575=CARTESIAN_POINT('',(1.7,-1.008,1.3));
#5576=CARTESIAN_POINT('',(1.7,-1.008,1.));
#5577=CARTESIAN_POINT('',(1.7,1.008,1.));
#5578=CARTESIAN_POINT('',(1.7,-1.15,1.));
#5579=CARTESIAN_POINT('',(1.7,1.008,1.3));
#5580=CARTESIAN_POINT('',(1.7,1.008,1.));
#5581=CARTESIAN_POINT('',(1.7,-1.15,1.3));
#5582=CARTESIAN_POINT('Origin',(1.25,0.,1.3));
#5583=CARTESIAN_POINT('',(1.95924336973479,-0.966521060842434,1.3));
#5584=CARTESIAN_POINT('',(0.709243369734789,1.16652106084243,1.3));
#5585=CARTESIAN_POINT('Origin',(2.5,0.88,3.));
#5586=CARTESIAN_POINT('',(2.5,0.88,2.3));
#5587=CARTESIAN_POINT('',(2.5,0.88,3.7));
#5588=CARTESIAN_POINT('Origin',(2.5,0.88,3.));
#5589=CARTESIAN_POINT('Origin',(2.5,0.88,3.));
#5590=CARTESIAN_POINT('Origin',(2.5,0.88,3.));
#5591=CARTESIAN_POINT('',(2.5,0.88,2.3));
#5592=CARTESIAN_POINT('Origin',(2.5,1.12,3.));
#5593=CARTESIAN_POINT('',(2.5,0.88,3.7));
#5594=CARTESIAN_POINT('Origin',(2.5,1.12,3.));
#5595=CARTESIAN_POINT('Origin',(2.5,0.88,3.));
#5596=CARTESIAN_POINT('Origin',(2.5,0.88,3.));
#5597=CARTESIAN_POINT('Origin',(0.,1.28,1.));
#5598=CARTESIAN_POINT('',(0.,1.28,1.));
#5599=CARTESIAN_POINT('',(0.,1.28,1.));
#5600=CARTESIAN_POINT('',(0.,1.28,1.));
#5601=CARTESIAN_POINT('',(2.5,0.88,1.));
#5602=CARTESIAN_POINT('',(0.,1.28,1.));
#5603=CARTESIAN_POINT('',(2.5,0.88,1.));
#5604=CARTESIAN_POINT('',(0.,1.28,3.7));
#5605=CARTESIAN_POINT('Origin',(2.5,0.88,1.));
#5606=CARTESIAN_POINT('',(2.5,0.88,1.));
#5607=CARTESIAN_POINT('Origin',(0.,1.52,1.));
#5608=CARTESIAN_POINT('',(0.,1.28,2.3));
#5609=CARTESIAN_POINT('',(0.,1.52,1.));
#5610=CARTESIAN_POINT('Origin',(1.25,1.2,3.7));
#5611=CARTESIAN_POINT('',(0.,1.28,3.7));
#5612=CARTESIAN_POINT('Origin',(0.,1.28,3.));
#5613=CARTESIAN_POINT('Origin',(0.,1.52,3.));
#5614=CARTESIAN_POINT('Origin',(0.,1.28,3.));
#5615=CARTESIAN_POINT('Origin',(0.,1.52,3.));
#5616=CARTESIAN_POINT('Origin',(0.,1.52,3.));
#5617=CARTESIAN_POINT('Origin',(2.5,-0.88,1.));
#5618=CARTESIAN_POINT('',(2.5,-0.88,3.7));
#5619=CARTESIAN_POINT('',(2.5,-0.88,3.7));
#5620=CARTESIAN_POINT('',(2.5,-0.88,2.3));
#5621=CARTESIAN_POINT('Origin',(2.5,-0.88,3.));
#5622=CARTESIAN_POINT('',(2.5,-0.88,1.));
#5623=CARTESIAN_POINT('',(2.5,-0.88,1.));
#5624=CARTESIAN_POINT('',(2.5,-0.88,1.));
#5625=CARTESIAN_POINT('',(0.,-1.28,1.));
#5626=CARTESIAN_POINT('',(2.5,-0.88,1.));
#5627=CARTESIAN_POINT('',(0.,-1.28,1.));
#5628=CARTESIAN_POINT('Origin',(2.5,-0.88,3.));
#5629=CARTESIAN_POINT('Origin',(2.5,-0.88,3.));
#5630=CARTESIAN_POINT('Origin',(2.5,-0.88,3.));
#5631=CARTESIAN_POINT('Origin',(2.5,-1.12,3.));
#5632=CARTESIAN_POINT('Origin',(2.5,-1.12,3.));
#5633=CARTESIAN_POINT('',(2.5,-1.12,2.3));
#5634=CARTESIAN_POINT('',(2.5,-1.12,3.7));
#5635=CARTESIAN_POINT('Origin',(2.5,-1.12,3.));
#5636=CARTESIAN_POINT('Origin',(2.5,-1.12,3.));
#5637=CARTESIAN_POINT('Origin',(2.5,-1.12,1.));
#5638=CARTESIAN_POINT('',(2.5,-1.12,1.));
#5639=CARTESIAN_POINT('Origin',(0.,-1.28,1.));
#5640=CARTESIAN_POINT('',(0.,-1.52,2.3));
#5641=CARTESIAN_POINT('',(0.,-1.28,1.));
#5642=CARTESIAN_POINT('Origin',(1.25,-1.2,3.7));
#5643=CARTESIAN_POINT('',(0.,-1.52,3.7));
#5644=CARTESIAN_POINT('Origin',(1.25,-1.2,1.));
#5645=CARTESIAN_POINT('Origin',(0.,-1.52,3.));
#5646=CARTESIAN_POINT('Origin',(0.,-1.52,3.));
#5647=CARTESIAN_POINT('Origin',(0.,-1.52,3.));
#5648=CARTESIAN_POINT('Origin',(0.,-1.52,3.));
#5649=CARTESIAN_POINT('Origin',(0.,-1.52,3.));
#5900=UNCERTAINTY_MEASURE_WITH_UNIT(LENGTH_MEASURE(0.001),#5930,
'DISTANCE_ACCURACY_VALUE',
'Maximum model space distance between geometric entities at asserted c
onnectivities');
#5905=UNCERTAINTY_MEASURE_WITH_UNIT(LENGTH_MEASURE(0.001),#5930,
'DISTANCE_ACCURACY_VALUE',
'Maximum model space distance between geometric entities at asserted c
onnectivities');
#5924=(
GEOMETRIC_REPRESENTATION_CONTEXT(3)
GLOBAL_UNCERTAINTY_ASSIGNED_CONTEXT((#5900))
GLOBAL_UNIT_ASSIGNED_CONTEXT((#5930,#5932,#5933))
REPRESENTATION_CONTEXT('','3D')
);
#5929=(
GEOMETRIC_REPRESENTATION_CONTEXT(3)
GLOBAL_UNCERTAINTY_ASSIGNED_CONTEXT((#5905))
GLOBAL_UNIT_ASSIGNED_CONTEXT((#5930,#5932,#5933))
REPRESENTATION_CONTEXT('','3D')
);
#5930=(
LENGTH_UNIT()
NAMED_UNIT(*)
SI_UNIT(.CENTI.,.METRE.)
);
#5932=(
NAMED_UNIT(*)
PLANE_ANGLE_UNIT()
SI_UNIT($,.RADIAN.)
);
#5933=(
NAMED_UNIT(*)
SI_UNIT($,.STERADIAN.)
SOLID_ANGLE_UNIT()
);
#5952=SHAPE_DEFINITION_REPRESENTATION(#5982,#6057);
#5982=PRODUCT_DEFINITION_SHAPE('',$,#6081);
#6057=SHAPE_REPRESENTATION('',(#3640),#5924);
#6062=PRODUCT_DEFINITION_CONTEXT('part definition',#6133,'design');
#6081=PRODUCT_DEFINITION('Offset cable chain link',
'Offset cable chain link',#6104,#6062);
#6104=PRODUCT_DEFINITION_FORMATION('',$,#6153);
#6133=APPLICATION_CONTEXT(
'Core Data for Automotive Mechanical Design Process');
#6134=PRODUCT_CONTEXT('part definition',#6133,'mechanical');
#6153=PRODUCT('Offset cable chain link','Offset cable chain link',
'Offset cable chain link',(#6134));
#6228=COLOUR_RGB('Off White',0.89,0.88,0.83);
#6229=FILL_AREA_STYLE_COLOUR('',#6228);
#6230=FILL_AREA_STYLE('',(#6229));
#6231=SURFACE_STYLE_FILL_AREA(#6230);
#6232=SURFACE_SIDE_STYLE('',(#6231));
#6233=SURFACE_STYLE_USAGE(.BOTH.,#6232);
#6234=PRESENTATION_STYLE_ASSIGNMENT((#6233));
ENDSEC;
END-ISO-10303-21;
